ISO-10303-21;
HEADER;
/* Generated by software containing ST-Developer
 * from STEP Tools, Inc. (www.steptools.com) 
 */

FILE_DESCRIPTION(
/* description */ ('Hand wheel with handle and shaft collar'),
/* implementation_level */ '2;1');

FILE_NAME(
/* name */ 'Balls (1).step',
/* time_stamp */ '2026-10-28T03:23:19-07:00',
/* author */ (''),
/* organization */ (''),
/* preprocessor_version */ 'ST-DEVELOPER v20.2',
/* originating_system */ 'Autodesk Translation Framework v15.17.0.0',
/* authorisation */ '');

FILE_SCHEMA (('AUTOMOTIVE_DESIGN { 1 0 10303 214 3 1 1 }'));
ENDSEC;

DATA;
#10=MECHANICAL_DESIGN_GEOMETRIC_PRESENTATION_REPRESENTATION('',(#428,#429,#430,#431,#432,#433,#434,#435),#10510);
#281=SPHERICAL_SURFACE('',#6234,0.23815);
#282=SPHERICAL_SURFACE('',#6236,0.23815);
#283=SPHERICAL_SURFACE('',#6238,0.23815);
#284=SPHERICAL_SURFACE('',#6240,0.23815);
#285=SPHERICAL_SURFACE('',#6242,0.23815);
#286=SPHERICAL_SURFACE('',#6244,0.23815);
#287=SPHERICAL_SURFACE('',#6246,0.23815);
#288=SPHERICAL_SURFACE('',#6248,0.23815);
#357=SHAPE_REPRESENTATION_RELATIONSHIP('SRR','None',#10676,#389);
#389=ADVANCED_BREP_SHAPE_REPRESENTATION('',(#473,#474,#475,#476,#477,#478,
#479,#480),#10503);
#428=STYLED_ITEM('',(#10908),#473);
#429=STYLED_ITEM('',(#10908),#474);
#430=STYLED_ITEM('',(#10908),#475);
#431=STYLED_ITEM('',(#10908),#476);
#432=STYLED_ITEM('',(#10908),#477);
#433=STYLED_ITEM('',(#10908),#478);
#434=STYLED_ITEM('',(#10908),#479);
#435=STYLED_ITEM('',(#10908),#480);
#473=MANIFOLD_SOLID_BREP('Body1',#5329);
#474=MANIFOLD_SOLID_BREP('Body2',#5330);
#475=MANIFOLD_SOLID_BREP('Body3',#5331);
#476=MANIFOLD_SOLID_BREP('Body4',#5332);
#477=MANIFOLD_SOLID_BREP('Body5',#5333);
#478=MANIFOLD_SOLID_BREP('Body6',#5334);
#479=MANIFOLD_SOLID_BREP('Body7',#5335);
#480=MANIFOLD_SOLID_BREP('Body8',#5336);
#1020=FACE_OUTER_BOUND('',#1440,.T.);
#1021=FACE_OUTER_BOUND('',#1441,.T.);
#1022=FACE_OUTER_BOUND('',#1442,.T.);
#1023=FACE_OUTER_BOUND('',#1443,.T.);
#1024=FACE_OUTER_BOUND('',#1444,.T.);
#1025=FACE_OUTER_BOUND('',#1445,.T.);
#1026=FACE_OUTER_BOUND('',#1446,.T.);
#1027=FACE_OUTER_BOUND('',#1447,.T.);
#1440=EDGE_LOOP('',(#4637,#4638));
#1441=EDGE_LOOP('',(#4639,#4640));
#1442=EDGE_LOOP('',(#4641,#4642));
#1443=EDGE_LOOP('',(#4643,#4644));
#1444=EDGE_LOOP('',(#4645,#4646));
#1445=EDGE_LOOP('',(#4647,#4648));
#1446=EDGE_LOOP('',(#4649,#4650));
#1447=EDGE_LOOP('',(#4651,#4652));
#2376=CIRCLE('',#6235,0.23815);
#2377=CIRCLE('',#6237,0.23815);
#2378=CIRCLE('',#6239,0.23815);
#2379=CIRCLE('',#6241,0.23815);
#2380=CIRCLE('',#6243,0.23815);
#2381=CIRCLE('',#6245,0.23815);
#2382=CIRCLE('',#6247,0.23815);
#2383=CIRCLE('',#6249,0.23815);
#2806=VERTEX_POINT('',#9768);
#2807=VERTEX_POINT('',#9769);
#2808=VERTEX_POINT('',#9772);
#2809=VERTEX_POINT('',#9773);
#2810=VERTEX_POINT('',#9776);
#2811=VERTEX_POINT('',#9777);
#2812=VERTEX_POINT('',#9780);
#2813=VERTEX_POINT('',#9781);
#2814=VERTEX_POINT('',#9784);
#2815=VERTEX_POINT('',#9785);
#2816=VERTEX_POINT('',#9788);
#2817=VERTEX_POINT('',#9789);
#2818=VERTEX_POINT('',#9792);
#2819=VERTEX_POINT('',#9793);
#2820=VERTEX_POINT('',#9796);
#2821=VERTEX_POINT('',#9797);
#3436=EDGE_CURVE('',#2806,#2807,#2376,.T.);
#3437=EDGE_CURVE('',#2808,#2809,#2377,.T.);
#3438=EDGE_CURVE('',#2810,#2811,#2378,.T.);
#3439=EDGE_CURVE('',#2812,#2813,#2379,.T.);
#3440=EDGE_CURVE('',#2814,#2815,#2380,.T.);
#3441=EDGE_CURVE('',#2816,#2817,#2381,.T.);
#3442=EDGE_CURVE('',#2818,#2819,#2382,.T.);
#3443=EDGE_CURVE('',#2820,#2821,#2383,.T.);
#4637=ORIENTED_EDGE('',*,*,#3436,.T.);
#4638=ORIENTED_EDGE('',*,*,#3436,.F.);
#4639=ORIENTED_EDGE('',*,*,#3437,.T.);
#4640=ORIENTED_EDGE('',*,*,#3437,.F.);
#4641=ORIENTED_EDGE('',*,*,#3438,.T.);
#4642=ORIENTED_EDGE('',*,*,#3438,.F.);
#4643=ORIENTED_EDGE('',*,*,#3439,.T.);
#4644=ORIENTED_EDGE('',*,*,#3439,.F.);
#4645=ORIENTED_EDGE('',*,*,#3440,.T.);
#4646=ORIENTED_EDGE('',*,*,#3440,.F.);
#4647=ORIENTED_EDGE('',*,*,#3441,.T.);
#4648=ORIENTED_EDGE('',*,*,#3441,.F.);
#4649=ORIENTED_EDGE('',*,*,#3442,.T.);
#4650=ORIENTED_EDGE('',*,*,#3442,.F.);
#4651=ORIENTED_EDGE('',*,*,#3443,.T.);
#4652=ORIENTED_EDGE('',*,*,#3443,.F.);
#5232=ADVANCED_FACE('',(#1020),#281,.T.);
#5233=ADVANCED_FACE('',(#1021),#282,.T.);
#5234=ADVANCED_FACE('',(#1022),#283,.T.);
#5235=ADVANCED_FACE('',(#1023),#284,.T.);
#5236=ADVANCED_FACE('',(#1024),#285,.T.);
#5237=ADVANCED_FACE('',(#1025),#286,.T.);
#5238=ADVANCED_FACE('',(#1026),#287,.T.);
#5239=ADVANCED_FACE('',(#1027),#288,.T.);
#5329=CLOSED_SHELL('',(#5232));
#5330=CLOSED_SHELL('',(#5233));
#5331=CLOSED_SHELL('',(#5234));
#5332=CLOSED_SHELL('',(#5235));
#5333=CLOSED_SHELL('',(#5236));
#5334=CLOSED_SHELL('',(#5237));
#5335=CLOSED_SHELL('',(#5238));
#5336=CLOSED_SHELL('',(#5239));
#6233=AXIS2_PLACEMENT_3D('',#9766,#7766,#7767);
#6234=AXIS2_PLACEMENT_3D('',#9767,#7768,#7769);
#6235=AXIS2_PLACEMENT_3D('',#9770,#7770,#7771);
#6236=AXIS2_PLACEMENT_3D('',#9771,#7772,#7773);
#6237=AXIS2_PLACEMENT_3D('',#9774,#7774,#7775);
#6238=AXIS2_PLACEMENT_3D('',#9775,#7776,#7777);
#6239=AXIS2_PLACEMENT_3D('',#9778,#7778,#7779);
#6240=AXIS2_PLACEMENT_3D('',#9779,#7780,#7781);
#6241=AXIS2_PLACEMENT_3D('',#9782,#7782,#7783);
#6242=AXIS2_PLACEMENT_3D('',#9783,#7784,#7785);
#6243=AXIS2_PLACEMENT_3D('',#9786,#7786,#7787);
#6244=AXIS2_PLACEMENT_3D('',#9787,#7788,#7789);
#6245=AXIS2_PLACEMENT_3D('',#9790,#7790,#7791);
#6246=AXIS2_PLACEMENT_3D('',#9791,#7792,#7793);
#6247=AXIS2_PLACEMENT_3D('',#9794,#7794,#7795);
#6248=AXIS2_PLACEMENT_3D('',#9795,#7796,#7797);
#6249=AXIS2_PLACEMENT_3D('',#9798,#7798,#7799);
#7766=DIRECTION('axis',(0.,0.,1.));
#7767=DIRECTION('refdir',(1.,0.,0.));
#7768=DIRECTION('center_axis',(0.,0.,1.));
#7769=DIRECTION('ref_axis',(1.,0.,0.));
#7770=DIRECTION('center_axis',(1.22464679914735E-16,-1.,0.));
#7771=DIRECTION('ref_axis',(-1.,-1.22464679914735E-16,0.));
#7772=DIRECTION('center_axis',(0.707106781186548,0.,0.707106781186548));
#7773=DIRECTION('ref_axis',(0.707106781186548,0.,-0.707106781186548));
#7774=DIRECTION('center_axis',(8.65956056235494E-17,-1.,-8.65956056235493E-17));
#7775=DIRECTION('ref_axis',(-0.707106781186547,-1.22464679914735E-16,0.707106781186547));
#7776=DIRECTION('center_axis',(1.,0.,0.));
#7777=DIRECTION('ref_axis',(6.12323399573676E-17,0.,-1.));
#7778=DIRECTION('center_axis',(7.49879891330929E-33,-1.,-1.22464679914735E-16));
#7779=DIRECTION('ref_axis',(-6.12323399573676E-17,-1.22464679914735E-16,
1.));
#7780=DIRECTION('center_axis',(0.707106781186548,0.,-0.707106781186548));
#7781=DIRECTION('ref_axis',(-0.707106781186548,0.,-0.707106781186548));
#7782=DIRECTION('center_axis',(-8.65956056235493E-17,-1.,-8.65956056235494E-17));
#7783=DIRECTION('ref_axis',(0.707106781186547,-1.22464679914735E-16,0.707106781186547));
#7784=DIRECTION('center_axis',(0.,0.,-1.));
#7785=DIRECTION('ref_axis',(-1.,0.,-1.22464679914735E-16));
#7786=DIRECTION('center_axis',(-1.22464679914735E-16,-1.,-1.49975978266186E-32));
#7787=DIRECTION('ref_axis',(1.,-1.22464679914735E-16,1.22464679914735E-16));
#7788=DIRECTION('center_axis',(-0.707106781186547,0.,-0.707106781186548));
#7789=DIRECTION('ref_axis',(-0.707106781186548,0.,0.707106781186547));
#7790=DIRECTION('center_axis',(-8.65956056235493E-17,-1.,8.65956056235493E-17));
#7791=DIRECTION('ref_axis',(0.707106781186548,-1.22464679914735E-16,-0.707106781186547));
#7792=DIRECTION('center_axis',(-1.,0.,0.));
#7793=DIRECTION('ref_axis',(-1.83697019872103E-16,0.,1.));
#7794=DIRECTION('center_axis',(-2.24963967399279E-32,-1.,1.22464679914735E-16));
#7795=DIRECTION('ref_axis',(1.83697019872103E-16,-1.22464679914735E-16,
-1.));
#7796=DIRECTION('center_axis',(-0.707106781186548,0.,0.707106781186548));
#7797=DIRECTION('ref_axis',(0.707106781186547,0.,0.707106781186548));
#7798=DIRECTION('center_axis',(8.65956056235493E-17,-1.,8.65956056235493E-17));
#7799=DIRECTION('ref_axis',(-0.707106781186547,-1.22464679914735E-16,-0.707106781186548));
#9766=CARTESIAN_POINT('',(0.,0.,0.));
#9767=CARTESIAN_POINT('Origin',(1.,0.,0.));
#9768=CARTESIAN_POINT('',(1.,-1.78583896120461E-33,0.23815));
#9769=CARTESIAN_POINT('',(1.,-1.78583896120461E-33,-0.23815));
#9770=CARTESIAN_POINT('Origin',(1.,0.,0.));
#9771=CARTESIAN_POINT('Origin',(0.707106781186548,0.,-0.707106781186547));
#9772=CARTESIAN_POINT('',(0.875504261126124,-1.78583896120461E-33,-0.538709301246971));
#9773=CARTESIAN_POINT('',(0.538709301246971,-1.78583896120461E-33,-0.875504261126124));
#9774=CARTESIAN_POINT('Origin',(0.707106781186548,0.,-0.707106781186547));
#9775=CARTESIAN_POINT('Origin',(6.12323399573677E-17,0.,-1.));
#9776=CARTESIAN_POINT('',(0.23815,-1.78583896120461E-33,-1.));
#9777=CARTESIAN_POINT('',(-0.23815,-1.78583896120461E-33,-1.));
#9778=CARTESIAN_POINT('Origin',(6.12323399573677E-17,0.,-1.));
#9779=CARTESIAN_POINT('Origin',(-0.707106781186547,0.,-0.707106781186548));
#9780=CARTESIAN_POINT('',(-0.538709301246971,-1.78583896120461E-33,-0.875504261126124));
#9781=CARTESIAN_POINT('',(-0.875504261126124,-1.78583896120461E-33,-0.538709301246971));
#9782=CARTESIAN_POINT('Origin',(-0.707106781186547,0.,-0.707106781186548));
#9783=CARTESIAN_POINT('Origin',(-1.,0.,-1.22464679914735E-16));
#9784=CARTESIAN_POINT('',(-1.,-1.78583896120461E-33,-0.23815));
#9785=CARTESIAN_POINT('',(-1.,-1.78583896120461E-33,0.23815));
#9786=CARTESIAN_POINT('Origin',(-1.,0.,-1.22464679914735E-16));
#9787=CARTESIAN_POINT('Origin',(-0.707106781186548,0.,0.707106781186547));
#9788=CARTESIAN_POINT('',(-0.875504261126124,-7.94881478324376E-33,0.538709301246971));
#9789=CARTESIAN_POINT('',(-0.538709301246971,4.37713686083455E-33,0.875504261126124));
#9790=CARTESIAN_POINT('Origin',(-0.707106781186548,0.,0.707106781186547));
#9791=CARTESIAN_POINT('Origin',(-1.83697019872103E-16,0.,1.));
#9792=CARTESIAN_POINT('',(-0.23815,-1.78583896120461E-33,1.));
#9793=CARTESIAN_POINT('',(0.23815,-1.78583896120461E-33,1.));
#9794=CARTESIAN_POINT('Origin',(-1.83697019872103E-16,0.,1.));
#9795=CARTESIAN_POINT('Origin',(0.707106781186547,0.,0.707106781186548));
#9796=CARTESIAN_POINT('',(0.538709301246971,-4.86732687222419E-33,0.875504261126124));
#9797=CARTESIAN_POINT('',(0.875504261126124,1.29564894981497E-33,0.538709301246971));
#9798=CARTESIAN_POINT('Origin',(0.707106781186547,0.,0.707106781186548));
#10464=UNCERTAINTY_MEASURE_WITH_UNIT(LENGTH_MEASURE(0.001),#10511,
'DISTANCE_ACCURACY_VALUE',
'Maximum model space distance between geometric entities at asserted c
onnectivities');
#10471=UNCERTAINTY_MEASURE_WITH_UNIT(LENGTH_MEASURE(0.001),#10511,
'DISTANCE_ACCURACY_VALUE',
'Maximum model space distance between geometric entities at asserted c
onnectivities');
#10503=(
GEOMETRIC_REPRESENTATION_CONTEXT(3)
GLOBAL_UNCERTAINTY_ASSIGNED_CONTEXT((#10464))
GLOBAL_UNIT_ASSIGNED_CONTEXT((#10511,#10513,#10514))
REPRESENTATION_CONTEXT('','3D')
);
#10510=(
GEOMETRIC_REPRESENTATION_CONTEXT(3)
GLOBAL_UNCERTAINTY_ASSIGNED_CONTEXT((#10471))
GLOBAL_UNIT_ASSIGNED_CONTEXT((#10511,#10513,#10514))
REPRESENTATION_CONTEXT('','3D')
);
#10511=(
LENGTH_UNIT()
NAMED_UNIT(*)
SI_UNIT(.CENTI.,.METRE.)
);
#10513=(
NAMED_UNIT(*)
PLANE_ANGLE_UNIT()
SI_UNIT($,.RADIAN.)
);
#10514=(
NAMED_UNIT(*)
SI_UNIT($,.STERADIAN.)
SOLID_ANGLE_UNIT()
);
#10546=SHAPE_DEFINITION_REPRESENTATION(#10589,#10676);
#10589=PRODUCT_DEFINITION_SHAPE('',$,#10715);
#10676=SHAPE_REPRESENTATION('',(#6233),#10503);
#10683=PRODUCT_DEFINITION_CONTEXT('part definition',#10799,'design');
#10715=PRODUCT_DEFINITION('Balls (1)','Balls (1)',#10753,#10683);
#10753=PRODUCT_DEFINITION_FORMATION('',$,#10832);
#10799=APPLICATION_CONTEXT(
'Core Data for Automotive Mechanical Design Process');
#10800=PRODUCT_CONTEXT('part definition',#10799,'mechanical');
#10832=PRODUCT('Balls (1)','Balls (1)','Balls (1)',(#10800));
#10902=COLOUR_RGB('Grey',0.48,0.52,0.57);
#10903=FILL_AREA_STYLE_COLOUR('',#10902);
#10904=FILL_AREA_STYLE('',(#10903));
#10905=SURFACE_STYLE_FILL_AREA(#10904);
#10906=SURFACE_SIDE_STYLE('',(#10905));
#10907=SURFACE_STYLE_USAGE(.BOTH.,#10906);
#10908=PRESENTATION_STYLE_ASSIGNMENT((#10907));
ENDSEC;
END-ISO-10303-21;
